ISO-10303-21;
HEADER;
/* Generated by software containing ST-Developer
 * from STEP Tools, Inc. (www.steptools.com) 
 */

FILE_DESCRIPTION(
/* description */ (''),
/* implementation_level */ '2;1');

FILE_NAME(
/* name */ 'Base.step',
/* time_stamp */ '2026-10-23T22:30:33+06:00',
/* author */ (''),
/* organization */ (''),
/* preprocessor_version */ 'ST-DEVELOPER v20.2',
/* originating_system */ 'Autodesk Translation Framework v15.15.0.0',
/* authorisation */ '');

FILE_SCHEMA (('AUTOMOTIVE_DESIGN { 1 0 10303 214 3 1 1 }'));
ENDSEC;

DATA;
#10=MECHANICAL_DESIGN_GEOMETRIC_PRESENTATION_REPRESENTATION('',(#235),#10131);
#215=SHAPE_REPRESENTATION_RELATIONSHIP('SRR','None',#10169,#225);
#225=ADVANCED_BREP_SHAPE_REPRESENTATION('',(#245),#10121);
#235=STYLED_ITEM('',(#10247),#245);
#245=MANIFOLD_SOLID_BREP('Base',#5879);
#255=FACE_BOUND('',#827,.T.);
#256=FACE_BOUND('',#828,.T.);
#257=FACE_BOUND('',#829,.T.);
#258=FACE_BOUND('',#830,.T.);
#259=FACE_BOUND('',#831,.T.);
#260=FACE_BOUND('',#832,.T.);
#261=FACE_BOUND('',#833,.T.);
#262=FACE_BOUND('',#834,.T.);
#263=FACE_BOUND('',#842,.T.);
#264=FACE_BOUND('',#843,.T.);
#265=FACE_BOUND('',#844,.T.);
#266=FACE_BOUND('',#845,.T.);
#267=FACE_BOUND('',#846,.T.);
#268=FACE_BOUND('',#847,.T.);
#269=FACE_BOUND('',#848,.T.);
#270=FACE_BOUND('',#849,.T.);
#324=PLANE('',#6029);
#325=PLANE('',#6030);
#326=PLANE('',#6036);
#327=PLANE('',#6041);
#328=PLANE('',#6042);
#329=PLANE('',#6043);
#467=FACE_OUTER_BOUND('',#816,.T.);
#468=FACE_OUTER_BOUND('',#817,.T.);
#469=FACE_OUTER_BOUND('',#818,.T.);
#470=FACE_OUTER_BOUND('',#819,.T.);
#471=FACE_OUTER_BOUND('',#820,.T.);
#472=FACE_OUTER_BOUND('',#821,.T.);
#473=FACE_OUTER_BOUND('',#822,.T.);
#474=FACE_OUTER_BOUND('',#823,.T.);
#475=FACE_OUTER_BOUND('',#824,.T.);
#476=FACE_OUTER_BOUND('',#825,.T.);
#477=FACE_OUTER_BOUND('',#826,.T.);
#478=FACE_OUTER_BOUND('',#835,.T.);
#479=FACE_OUTER_BOUND('',#836,.T.);
#480=FACE_OUTER_BOUND('',#837,.T.);
#481=FACE_OUTER_BOUND('',#838,.T.);
#482=FACE_OUTER_BOUND('',#839,.T.);
#483=FACE_OUTER_BOUND('',#840,.T.);
#484=FACE_OUTER_BOUND('',#841,.T.);
#816=EDGE_LOOP('',(#3716,#3717,#3718,#3719));
#817=EDGE_LOOP('',(#3720,#3721,#3722,#3723));
#818=EDGE_LOOP('',(#3724,#3725,#3726,#3727));
#819=EDGE_LOOP('',(#3728,#3729,#3730,#3731));
#820=EDGE_LOOP('',(#3732,#3733,#3734,#3735));
#821=EDGE_LOOP('',(#3736,#3737,#3738,#3739));
#822=EDGE_LOOP('',(#3740,#3741,#3742,#3743));
#823=EDGE_LOOP('',(#3744,#3745,#3746,#3747));
#824=EDGE_LOOP('',(#3748,#3749,#3750,#3751));
#825=EDGE_LOOP('',(#3752,#3753,#3754,#3755));
#826=EDGE_LOOP('',(#3756,#3757,#3758,#3759,#3760,#3761,#3762,#3763));
#827=EDGE_LOOP('',(#3764));
#828=EDGE_LOOP('',(#3765));
#829=EDGE_LOOP('',(#3766));
#830=EDGE_LOOP('',(#3767));
#831=EDGE_LOOP('',(#3768));
#832=EDGE_LOOP('',(#3769));
#833=EDGE_LOOP('',(#3770));
#834=EDGE_LOOP('',(#3771));
#835=EDGE_LOOP('',(#3772,#3773,#3774,#3775));
#836=EDGE_LOOP('',(#3776,#3777,#3778,#3779));
#837=EDGE_LOOP('',(#3780,#3781,#3782,#3783));
#838=EDGE_LOOP('',(#3784,#3785,#3786,#3787));
#839=EDGE_LOOP('',(#3788,#3789,#3790,#3791));
#840=EDGE_LOOP('',(#3792,#3793,#3794,#3795));
#841=EDGE_LOOP('',(#3796,#3797,#3798,#3799,#3800,#3801,#3802,#3803));
#842=EDGE_LOOP('',(#3804));
#843=EDGE_LOOP('',(#3805));
#844=EDGE_LOOP('',(#3806));
#845=EDGE_LOOP('',(#3807));
#846=EDGE_LOOP('',(#3808));
#847=EDGE_LOOP('',(#3809));
#848=EDGE_LOOP('',(#3810));
#849=EDGE_LOOP('',(#3811));
#1234=LINE('',#8422,#1784);
#1235=LINE('',#8428,#1785);
#1236=LINE('',#8434,#1786);
#1237=LINE('',#8440,#1787);
#1238=LINE('',#8446,#1788);
#1239=LINE('',#8452,#1789);
#1240=LINE('',#8458,#1790);
#1241=LINE('',#8464,#1791);
#1242=LINE('',#8471,#1792);
#1243=LINE('',#8474,#1793);
#1244=LINE('',#8477,#1794);
#1245=LINE('',#8479,#1795);
#1246=LINE('',#8480,#1796);
#1247=LINE('',#8483,#1797);
#1248=LINE('',#8487,#1798);
#1249=LINE('',#8491,#1799);
#1250=LINE('',#8497,#1800);
#1251=LINE('',#8498,#1801);
#1252=LINE('',#8501,#1802);
#1253=LINE('',#8502,#1803);
#1254=LINE('',#8506,#1804);
#1255=LINE('',#8510,#1805);
#1256=LINE('',#8512,#1806);
#1257=LINE('',#8514,#1807);
#1784=VECTOR('',#6630,10.);
#1785=VECTOR('',#6637,10.);
#1786=VECTOR('',#6644,10.);
#1787=VECTOR('',#6651,10.);
#1788=VECTOR('',#6658,10.);
#1789=VECTOR('',#6665,10.);
#1790=VECTOR('',#6672,10.);
#1791=VECTOR('',#6679,10.);
#1792=VECTOR('',#6686,10.);
#1793=VECTOR('',#6689,10.);
#1794=VECTOR('',#6692,10.);
#1795=VECTOR('',#6693,10.);
#1796=VECTOR('',#6694,10.);
#1797=VECTOR('',#6697,10.);
#1798=VECTOR('',#6700,10.);
#1799=VECTOR('',#6703,10.);
#1800=VECTOR('',#6710,10.);
#1801=VECTOR('',#6711,10.);
#1802=VECTOR('',#6714,10.);
#1803=VECTOR('',#6715,10.);
#1804=VECTOR('',#6720,10.);
#1805=VECTOR('',#6725,10.);
#1806=VECTOR('',#6728,10.);
#1807=VECTOR('',#6731,10.);
#2334=CIRCLE('',#6003,10.);
#2335=CIRCLE('',#6004,10.);
#2336=CIRCLE('',#6006,10.);
#2337=CIRCLE('',#6007,10.);
#2338=CIRCLE('',#6009,10.);
#2339=CIRCLE('',#6010,10.);
#2340=CIRCLE('',#6012,10.);
#2341=CIRCLE('',#6013,10.);
#2342=CIRCLE('',#6015,10.);
#2343=CIRCLE('',#6016,10.);
#2344=CIRCLE('',#6018,10.);
#2345=CIRCLE('',#6019,10.);
#2346=CIRCLE('',#6021,10.);
#2347=CIRCLE('',#6022,10.);
#2348=CIRCLE('',#6024,10.);
#2349=CIRCLE('',#6025,10.);
#2350=CIRCLE('',#6027,10.);
#2351=CIRCLE('',#6028,10.);
#2352=CIRCLE('',#6031,10.);
#2353=CIRCLE('',#6032,10.);
#2354=CIRCLE('',#6033,10.);
#2355=CIRCLE('',#6035,10.);
#2356=CIRCLE('',#6038,10.);
#2357=CIRCLE('',#6040,10.);
#2430=VERTEX_POINT('',#8419);
#2431=VERTEX_POINT('',#8421);
#2432=VERTEX_POINT('',#8425);
#2433=VERTEX_POINT('',#8427);
#2434=VERTEX_POINT('',#8431);
#2435=VERTEX_POINT('',#8433);
#2436=VERTEX_POINT('',#8437);
#2437=VERTEX_POINT('',#8439);
#2438=VERTEX_POINT('',#8443);
#2439=VERTEX_POINT('',#8445);
#2440=VERTEX_POINT('',#8449);
#2441=VERTEX_POINT('',#8451);
#2442=VERTEX_POINT('',#8455);
#2443=VERTEX_POINT('',#8457);
#2444=VERTEX_POINT('',#8461);
#2445=VERTEX_POINT('',#8463);
#2446=VERTEX_POINT('',#8467);
#2447=VERTEX_POINT('',#8468);
#2448=VERTEX_POINT('',#8470);
#2449=VERTEX_POINT('',#8472);
#2450=VERTEX_POINT('',#8476);
#2451=VERTEX_POINT('',#8478);
#2452=VERTEX_POINT('',#8482);
#2453=VERTEX_POINT('',#8484);
#2454=VERTEX_POINT('',#8486);
#2455=VERTEX_POINT('',#8488);
#2456=VERTEX_POINT('',#8490);
#2457=VERTEX_POINT('',#8494);
#2458=VERTEX_POINT('',#8495);
#2459=VERTEX_POINT('',#8500);
#2460=VERTEX_POINT('',#8504);
#2461=VERTEX_POINT('',#8508);
#2910=EDGE_CURVE('',#2430,#2430,#2334,.T.);
#2911=EDGE_CURVE('',#2430,#2431,#1234,.T.);
#2912=EDGE_CURVE('',#2431,#2431,#2335,.T.);
#2913=EDGE_CURVE('',#2432,#2432,#2336,.T.);
#2914=EDGE_CURVE('',#2432,#2433,#1235,.T.);
#2915=EDGE_CURVE('',#2433,#2433,#2337,.T.);
#2916=EDGE_CURVE('',#2434,#2434,#2338,.T.);
#2917=EDGE_CURVE('',#2434,#2435,#1236,.T.);
#2918=EDGE_CURVE('',#2435,#2435,#2339,.T.);
#2919=EDGE_CURVE('',#2436,#2436,#2340,.T.);
#2920=EDGE_CURVE('',#2436,#2437,#1237,.T.);
#2921=EDGE_CURVE('',#2437,#2437,#2341,.T.);
#2922=EDGE_CURVE('',#2438,#2438,#2342,.T.);
#2923=EDGE_CURVE('',#2438,#2439,#1238,.T.);
#2924=EDGE_CURVE('',#2439,#2439,#2343,.T.);
#2925=EDGE_CURVE('',#2440,#2440,#2344,.T.);
#2926=EDGE_CURVE('',#2440,#2441,#1239,.T.);
#2927=EDGE_CURVE('',#2441,#2441,#2345,.T.);
#2928=EDGE_CURVE('',#2442,#2442,#2346,.T.);
#2929=EDGE_CURVE('',#2442,#2443,#1240,.T.);
#2930=EDGE_CURVE('',#2443,#2443,#2347,.T.);
#2931=EDGE_CURVE('',#2444,#2444,#2348,.T.);
#2932=EDGE_CURVE('',#2444,#2445,#1241,.T.);
#2933=EDGE_CURVE('',#2445,#2445,#2349,.T.);
#2934=EDGE_CURVE('',#2446,#2447,#2350,.T.);
#2935=EDGE_CURVE('',#2447,#2448,#1242,.T.);
#2936=EDGE_CURVE('',#2448,#2449,#2351,.T.);
#2937=EDGE_CURVE('',#2449,#2446,#1243,.T.);
#2938=EDGE_CURVE('',#2450,#2449,#1244,.T.);
#2939=EDGE_CURVE('',#2451,#2450,#1245,.T.);
#2940=EDGE_CURVE('',#2446,#2451,#1246,.T.);
#2941=EDGE_CURVE('',#2448,#2452,#1247,.T.);
#2942=EDGE_CURVE('',#2453,#2452,#2352,.T.);
#2943=EDGE_CURVE('',#2453,#2454,#1248,.T.);
#2944=EDGE_CURVE('',#2455,#2454,#2353,.T.);
#2945=EDGE_CURVE('',#2455,#2456,#1249,.T.);
#2946=EDGE_CURVE('',#2450,#2456,#2354,.T.);
#2947=EDGE_CURVE('',#2457,#2458,#2355,.T.);
#2948=EDGE_CURVE('',#2458,#2453,#1250,.T.);
#2949=EDGE_CURVE('',#2452,#2457,#1251,.T.);
#2950=EDGE_CURVE('',#2459,#2458,#1252,.T.);
#2951=EDGE_CURVE('',#2454,#2459,#1253,.T.);
#2952=EDGE_CURVE('',#2459,#2460,#2356,.T.);
#2953=EDGE_CURVE('',#2460,#2455,#1254,.T.);
#2954=EDGE_CURVE('',#2461,#2451,#2357,.T.);
#2955=EDGE_CURVE('',#2456,#2461,#1255,.T.);
#2956=EDGE_CURVE('',#2461,#2460,#1256,.T.);
#2957=EDGE_CURVE('',#2457,#2447,#1257,.T.);
#3716=ORIENTED_EDGE('',*,*,#2910,.F.);
#3717=ORIENTED_EDGE('',*,*,#2911,.T.);
#3718=ORIENTED_EDGE('',*,*,#2912,.F.);
#3719=ORIENTED_EDGE('',*,*,#2911,.F.);
#3720=ORIENTED_EDGE('',*,*,#2913,.F.);
#3721=ORIENTED_EDGE('',*,*,#2914,.T.);
#3722=ORIENTED_EDGE('',*,*,#2915,.F.);
#3723=ORIENTED_EDGE('',*,*,#2914,.F.);
#3724=ORIENTED_EDGE('',*,*,#2916,.F.);
#3725=ORIENTED_EDGE('',*,*,#2917,.T.);
#3726=ORIENTED_EDGE('',*,*,#2918,.F.);
#3727=ORIENTED_EDGE('',*,*,#2917,.F.);
#3728=ORIENTED_EDGE('',*,*,#2919,.F.);
#3729=ORIENTED_EDGE('',*,*,#2920,.T.);
#3730=ORIENTED_EDGE('',*,*,#2921,.F.);
#3731=ORIENTED_EDGE('',*,*,#2920,.F.);
#3732=ORIENTED_EDGE('',*,*,#2922,.F.);
#3733=ORIENTED_EDGE('',*,*,#2923,.T.);
#3734=ORIENTED_EDGE('',*,*,#2924,.F.);
#3735=ORIENTED_EDGE('',*,*,#2923,.F.);
#3736=ORIENTED_EDGE('',*,*,#2925,.F.);
#3737=ORIENTED_EDGE('',*,*,#2926,.T.);
#3738=ORIENTED_EDGE('',*,*,#2927,.F.);
#3739=ORIENTED_EDGE('',*,*,#2926,.F.);
#3740=ORIENTED_EDGE('',*,*,#2928,.F.);
#3741=ORIENTED_EDGE('',*,*,#2929,.T.);
#3742=ORIENTED_EDGE('',*,*,#2930,.F.);
#3743=ORIENTED_EDGE('',*,*,#2929,.F.);
#3744=ORIENTED_EDGE('',*,*,#2931,.F.);
#3745=ORIENTED_EDGE('',*,*,#2932,.T.);
#3746=ORIENTED_EDGE('',*,*,#2933,.F.);
#3747=ORIENTED_EDGE('',*,*,#2932,.F.);
#3748=ORIENTED_EDGE('',*,*,#2934,.T.);
#3749=ORIENTED_EDGE('',*,*,#2935,.T.);
#3750=ORIENTED_EDGE('',*,*,#2936,.T.);
#3751=ORIENTED_EDGE('',*,*,#2937,.T.);
#3752=ORIENTED_EDGE('',*,*,#2937,.F.);
#3753=ORIENTED_EDGE('',*,*,#2938,.F.);
#3754=ORIENTED_EDGE('',*,*,#2939,.F.);
#3755=ORIENTED_EDGE('',*,*,#2940,.F.);
#3756=ORIENTED_EDGE('',*,*,#2936,.F.);
#3757=ORIENTED_EDGE('',*,*,#2941,.T.);
#3758=ORIENTED_EDGE('',*,*,#2942,.F.);
#3759=ORIENTED_EDGE('',*,*,#2943,.T.);
#3760=ORIENTED_EDGE('',*,*,#2944,.F.);
#3761=ORIENTED_EDGE('',*,*,#2945,.T.);
#3762=ORIENTED_EDGE('',*,*,#2946,.F.);
#3763=ORIENTED_EDGE('',*,*,#2938,.T.);
#3764=ORIENTED_EDGE('',*,*,#2933,.T.);
#3765=ORIENTED_EDGE('',*,*,#2930,.T.);
#3766=ORIENTED_EDGE('',*,*,#2927,.T.);
#3767=ORIENTED_EDGE('',*,*,#2924,.T.);
#3768=ORIENTED_EDGE('',*,*,#2921,.T.);
#3769=ORIENTED_EDGE('',*,*,#2918,.T.);
#3770=ORIENTED_EDGE('',*,*,#2915,.T.);
#3771=ORIENTED_EDGE('',*,*,#2912,.T.);
#3772=ORIENTED_EDGE('',*,*,#2947,.T.);
#3773=ORIENTED_EDGE('',*,*,#2948,.T.);
#3774=ORIENTED_EDGE('',*,*,#2942,.T.);
#3775=ORIENTED_EDGE('',*,*,#2949,.T.);
#3776=ORIENTED_EDGE('',*,*,#2948,.F.);
#3777=ORIENTED_EDGE('',*,*,#2950,.F.);
#3778=ORIENTED_EDGE('',*,*,#2951,.F.);
#3779=ORIENTED_EDGE('',*,*,#2943,.F.);
#3780=ORIENTED_EDGE('',*,*,#2952,.T.);
#3781=ORIENTED_EDGE('',*,*,#2953,.T.);
#3782=ORIENTED_EDGE('',*,*,#2944,.T.);
#3783=ORIENTED_EDGE('',*,*,#2951,.T.);
#3784=ORIENTED_EDGE('',*,*,#2954,.T.);
#3785=ORIENTED_EDGE('',*,*,#2939,.T.);
#3786=ORIENTED_EDGE('',*,*,#2946,.T.);
#3787=ORIENTED_EDGE('',*,*,#2955,.T.);
#3788=ORIENTED_EDGE('',*,*,#2953,.F.);
#3789=ORIENTED_EDGE('',*,*,#2956,.F.);
#3790=ORIENTED_EDGE('',*,*,#2955,.F.);
#3791=ORIENTED_EDGE('',*,*,#2945,.F.);
#3792=ORIENTED_EDGE('',*,*,#2935,.F.);
#3793=ORIENTED_EDGE('',*,*,#2957,.F.);
#3794=ORIENTED_EDGE('',*,*,#2949,.F.);
#3795=ORIENTED_EDGE('',*,*,#2941,.F.);
#3796=ORIENTED_EDGE('',*,*,#2934,.F.);
#3797=ORIENTED_EDGE('',*,*,#2940,.T.);
#3798=ORIENTED_EDGE('',*,*,#2954,.F.);
#3799=ORIENTED_EDGE('',*,*,#2956,.T.);
#3800=ORIENTED_EDGE('',*,*,#2952,.F.);
#3801=ORIENTED_EDGE('',*,*,#2950,.T.);
#3802=ORIENTED_EDGE('',*,*,#2947,.F.);
#3803=ORIENTED_EDGE('',*,*,#2957,.T.);
#3804=ORIENTED_EDGE('',*,*,#2931,.T.);
#3805=ORIENTED_EDGE('',*,*,#2928,.T.);
#3806=ORIENTED_EDGE('',*,*,#2925,.T.);
#3807=ORIENTED_EDGE('',*,*,#2922,.T.);
#3808=ORIENTED_EDGE('',*,*,#2919,.T.);
#3809=ORIENTED_EDGE('',*,*,#2916,.T.);
#3810=ORIENTED_EDGE('',*,*,#2913,.T.);
#3811=ORIENTED_EDGE('',*,*,#2910,.T.);
#5328=CYLINDRICAL_SURFACE('',#6002,10.);
#5329=CYLINDRICAL_SURFACE('',#6005,10.);
#5330=CYLINDRICAL_SURFACE('',#6008,10.);
#5331=CYLINDRICAL_SURFACE('',#6011,10.);
#5332=CYLINDRICAL_SURFACE('',#6014,10.);
#5333=CYLINDRICAL_SURFACE('',#6017,10.);
#5334=CYLINDRICAL_SURFACE('',#6020,10.);
#5335=CYLINDRICAL_SURFACE('',#6023,10.);
#5336=CYLINDRICAL_SURFACE('',#6026,10.);
#5337=CYLINDRICAL_SURFACE('',#6034,10.);
#5338=CYLINDRICAL_SURFACE('',#6037,10.);
#5339=CYLINDRICAL_SURFACE('',#6039,10.);
#5530=ADVANCED_FACE('',(#467),#5328,.F.);
#5531=ADVANCED_FACE('',(#468),#5329,.F.);
#5532=ADVANCED_FACE('',(#469),#5330,.F.);
#5533=ADVANCED_FACE('',(#470),#5331,.F.);
#5534=ADVANCED_FACE('',(#471),#5332,.F.);
#5535=ADVANCED_FACE('',(#472),#5333,.F.);
#5536=ADVANCED_FACE('',(#473),#5334,.F.);
#5537=ADVANCED_FACE('',(#474),#5335,.F.);
#5538=ADVANCED_FACE('',(#475),#5336,.T.);
#5539=ADVANCED_FACE('',(#476),#324,.T.);
#5540=ADVANCED_FACE('',(#477,#255,#256,#257,#258,#259,#260,#261,#262),#325,
 .F.);
#5541=ADVANCED_FACE('',(#478),#5337,.T.);
#5542=ADVANCED_FACE('',(#479),#326,.T.);
#5543=ADVANCED_FACE('',(#480),#5338,.T.);
#5544=ADVANCED_FACE('',(#481),#5339,.T.);
#5545=ADVANCED_FACE('',(#482),#327,.T.);
#5546=ADVANCED_FACE('',(#483),#328,.T.);
#5547=ADVANCED_FACE('',(#484,#263,#264,#265,#266,#267,#268,#269,#270),#329,
 .T.);
#5879=CLOSED_SHELL('',(#5530,#5531,#5532,#5533,#5534,#5535,#5536,#5537,
#5538,#5539,#5540,#5541,#5542,#5543,#5544,#5545,#5546,#5547));
#6001=AXIS2_PLACEMENT_3D('',#8417,#6624,#6625);
#6002=AXIS2_PLACEMENT_3D('',#8418,#6626,#6627);
#6003=AXIS2_PLACEMENT_3D('',#8420,#6628,#6629);
#6004=AXIS2_PLACEMENT_3D('',#8423,#6631,#6632);
#6005=AXIS2_PLACEMENT_3D('',#8424,#6633,#6634);
#6006=AXIS2_PLACEMENT_3D('',#8426,#6635,#6636);
#6007=AXIS2_PLACEMENT_3D('',#8429,#6638,#6639);
#6008=AXIS2_PLACEMENT_3D('',#8430,#6640,#6641);
#6009=AXIS2_PLACEMENT_3D('',#8432,#6642,#6643);
#6010=AXIS2_PLACEMENT_3D('',#8435,#6645,#6646);
#6011=AXIS2_PLACEMENT_3D('',#8436,#6647,#6648);
#6012=AXIS2_PLACEMENT_3D('',#8438,#6649,#6650);
#6013=AXIS2_PLACEMENT_3D('',#8441,#6652,#6653);
#6014=AXIS2_PLACEMENT_3D('',#8442,#6654,#6655);
#6015=AXIS2_PLACEMENT_3D('',#8444,#6656,#6657);
#6016=AXIS2_PLACEMENT_3D('',#8447,#6659,#6660);
#6017=AXIS2_PLACEMENT_3D('',#8448,#6661,#6662);
#6018=AXIS2_PLACEMENT_3D('',#8450,#6663,#6664);
#6019=AXIS2_PLACEMENT_3D('',#8453,#6666,#6667);
#6020=AXIS2_PLACEMENT_3D('',#8454,#6668,#6669);
#6021=AXIS2_PLACEMENT_3D('',#8456,#6670,#6671);
#6022=AXIS2_PLACEMENT_3D('',#8459,#6673,#6674);
#6023=AXIS2_PLACEMENT_3D('',#8460,#6675,#6676);
#6024=AXIS2_PLACEMENT_3D('',#8462,#6677,#6678);
#6025=AXIS2_PLACEMENT_3D('',#8465,#6680,#6681);
#6026=AXIS2_PLACEMENT_3D('',#8466,#6682,#6683);
#6027=AXIS2_PLACEMENT_3D('',#8469,#6684,#6685);
#6028=AXIS2_PLACEMENT_3D('',#8473,#6687,#6688);
#6029=AXIS2_PLACEMENT_3D('',#8475,#6690,#6691);
#6030=AXIS2_PLACEMENT_3D('',#8481,#6695,#6696);
#6031=AXIS2_PLACEMENT_3D('',#8485,#6698,#6699);
#6032=AXIS2_PLACEMENT_3D('',#8489,#6701,#6702);
#6033=AXIS2_PLACEMENT_3D('',#8492,#6704,#6705);
#6034=AXIS2_PLACEMENT_3D('',#8493,#6706,#6707);
#6035=AXIS2_PLACEMENT_3D('',#8496,#6708,#6709);
#6036=AXIS2_PLACEMENT_3D('',#8499,#6712,#6713);
#6037=AXIS2_PLACEMENT_3D('',#8503,#6716,#6717);
#6038=AXIS2_PLACEMENT_3D('',#8505,#6718,#6719);
#6039=AXIS2_PLACEMENT_3D('',#8507,#6721,#6722);
#6040=AXIS2_PLACEMENT_3D('',#8509,#6723,#6724);
#6041=AXIS2_PLACEMENT_3D('',#8511,#6726,#6727);
#6042=AXIS2_PLACEMENT_3D('',#8513,#6729,#6730);
#6043=AXIS2_PLACEMENT_3D('',#8515,#6732,#6733);
#6624=DIRECTION('axis',(0.,0.,1.));
#6625=DIRECTION('refdir',(1.,0.,0.));
#6626=DIRECTION('center_axis',(0.,0.,-1.));
#6627=DIRECTION('ref_axis',(1.83697019872103E-16,1.,0.));
#6628=DIRECTION('center_axis',(0.,0.,-1.));
#6629=DIRECTION('ref_axis',(1.83697019872103E-16,1.,0.));
#6630=DIRECTION('',(0.,0.,-1.));
#6631=DIRECTION('center_axis',(0.,0.,1.));
#6632=DIRECTION('ref_axis',(1.83697019872103E-16,1.,0.));
#6633=DIRECTION('center_axis',(0.,0.,-1.));
#6634=DIRECTION('ref_axis',(1.83697019872103E-16,1.,0.));
#6635=DIRECTION('center_axis',(0.,0.,-1.));
#6636=DIRECTION('ref_axis',(1.83697019872103E-16,1.,0.));
#6637=DIRECTION('',(0.,0.,-1.));
#6638=DIRECTION('center_axis',(0.,0.,1.));
#6639=DIRECTION('ref_axis',(1.83697019872103E-16,1.,0.));
#6640=DIRECTION('center_axis',(0.,0.,-1.));
#6641=DIRECTION('ref_axis',(1.,-1.22464679914735E-16,0.));
#6642=DIRECTION('center_axis',(0.,0.,-1.));
#6643=DIRECTION('ref_axis',(1.,-1.22464679914735E-16,0.));
#6644=DIRECTION('',(0.,0.,-1.));
#6645=DIRECTION('center_axis',(0.,0.,1.));
#6646=DIRECTION('ref_axis',(1.,-1.22464679914735E-16,0.));
#6647=DIRECTION('center_axis',(0.,0.,-1.));
#6648=DIRECTION('ref_axis',(1.,-1.22464679914735E-16,0.));
#6649=DIRECTION('center_axis',(0.,0.,-1.));
#6650=DIRECTION('ref_axis',(1.,-1.22464679914735E-16,0.));
#6651=DIRECTION('',(0.,0.,-1.));
#6652=DIRECTION('center_axis',(0.,0.,1.));
#6653=DIRECTION('ref_axis',(1.,-1.22464679914735E-16,0.));
#6654=DIRECTION('center_axis',(0.,0.,-1.));
#6655=DIRECTION('ref_axis',(-6.12323399573677E-17,-1.,0.));
#6656=DIRECTION('center_axis',(0.,0.,-1.));
#6657=DIRECTION('ref_axis',(-6.12323399573677E-17,-1.,0.));
#6658=DIRECTION('',(0.,0.,-1.));
#6659=DIRECTION('center_axis',(0.,0.,1.));
#6660=DIRECTION('ref_axis',(-6.12323399573677E-17,-1.,0.));
#6661=DIRECTION('center_axis',(0.,0.,-1.));
#6662=DIRECTION('ref_axis',(-6.12323399573677E-17,-1.,0.));
#6663=DIRECTION('center_axis',(0.,0.,-1.));
#6664=DIRECTION('ref_axis',(-6.12323399573677E-17,-1.,0.));
#6665=DIRECTION('',(0.,0.,-1.));
#6666=DIRECTION('center_axis',(0.,0.,1.));
#6667=DIRECTION('ref_axis',(-6.12323399573677E-17,-1.,0.));
#6668=DIRECTION('center_axis',(0.,0.,-1.));
#6669=DIRECTION('ref_axis',(-1.,0.,0.));
#6670=DIRECTION('center_axis',(0.,0.,-1.));
#6671=DIRECTION('ref_axis',(-1.,0.,0.));
#6672=DIRECTION('',(0.,0.,-1.));
#6673=DIRECTION('center_axis',(0.,0.,1.));
#6674=DIRECTION('ref_axis',(-1.,0.,0.));
#6675=DIRECTION('center_axis',(0.,0.,-1.));
#6676=DIRECTION('ref_axis',(-1.,0.,0.));
#6677=DIRECTION('center_axis',(0.,0.,-1.));
#6678=DIRECTION('ref_axis',(-1.,0.,0.));
#6679=DIRECTION('',(0.,0.,-1.));
#6680=DIRECTION('center_axis',(0.,0.,1.));
#6681=DIRECTION('ref_axis',(-1.,0.,0.));
#6682=DIRECTION('center_axis',(0.,0.,1.));
#6683=DIRECTION('ref_axis',(-0.707106781186547,0.707106781186547,0.));
#6684=DIRECTION('center_axis',(0.,0.,-1.));
#6685=DIRECTION('ref_axis',(-0.707106781186547,0.707106781186547,0.));
#6686=DIRECTION('',(0.,0.,-1.));
#6687=DIRECTION('center_axis',(0.,0.,1.));
#6688=DIRECTION('ref_axis',(-0.707106781186547,0.707106781186547,0.));
#6689=DIRECTION('',(0.,0.,1.));
#6690=DIRECTION('center_axis',(-1.,0.,0.));
#6691=DIRECTION('ref_axis',(0.,-1.,0.));
#6692=DIRECTION('',(0.,1.,0.));
#6693=DIRECTION('',(0.,0.,-1.));
#6694=DIRECTION('',(0.,-1.,0.));
#6695=DIRECTION('center_axis',(0.,0.,1.));
#6696=DIRECTION('ref_axis',(1.,0.,0.));
#6697=DIRECTION('',(1.,0.,0.));
#6698=DIRECTION('center_axis',(0.,0.,1.));
#6699=DIRECTION('ref_axis',(0.707106781186547,0.707106781186547,0.));
#6700=DIRECTION('',(0.,-1.,0.));
#6701=DIRECTION('center_axis',(0.,0.,1.));
#6702=DIRECTION('ref_axis',(0.707106781186547,-0.707106781186547,0.));
#6703=DIRECTION('',(-1.,0.,0.));
#6704=DIRECTION('center_axis',(0.,0.,1.));
#6705=DIRECTION('ref_axis',(-0.707106781186547,-0.707106781186547,0.));
#6706=DIRECTION('center_axis',(0.,0.,1.));
#6707=DIRECTION('ref_axis',(0.707106781186547,0.707106781186547,0.));
#6708=DIRECTION('center_axis',(0.,0.,-1.));
#6709=DIRECTION('ref_axis',(0.707106781186547,0.707106781186547,0.));
#6710=DIRECTION('',(0.,0.,-1.));
#6711=DIRECTION('',(0.,0.,1.));
#6712=DIRECTION('center_axis',(1.,0.,0.));
#6713=DIRECTION('ref_axis',(0.,1.,0.));
#6714=DIRECTION('',(0.,1.,0.));
#6715=DIRECTION('',(0.,0.,1.));
#6716=DIRECTION('center_axis',(0.,0.,1.));
#6717=DIRECTION('ref_axis',(0.707106781186547,-0.707106781186547,0.));
#6718=DIRECTION('center_axis',(0.,0.,-1.));
#6719=DIRECTION('ref_axis',(0.707106781186547,-0.707106781186547,0.));
#6720=DIRECTION('',(0.,0.,-1.));
#6721=DIRECTION('center_axis',(0.,0.,1.));
#6722=DIRECTION('ref_axis',(-0.707106781186547,-0.707106781186547,0.));
#6723=DIRECTION('center_axis',(0.,0.,-1.));
#6724=DIRECTION('ref_axis',(-0.707106781186547,-0.707106781186547,0.));
#6725=DIRECTION('',(0.,0.,1.));
#6726=DIRECTION('center_axis',(0.,-1.,0.));
#6727=DIRECTION('ref_axis',(1.,0.,0.));
#6728=DIRECTION('',(1.,0.,0.));
#6729=DIRECTION('center_axis',(0.,1.,0.));
#6730=DIRECTION('ref_axis',(-1.,0.,0.));
#6731=DIRECTION('',(-1.,0.,0.));
#6732=DIRECTION('center_axis',(0.,0.,1.));
#6733=DIRECTION('ref_axis',(1.,0.,0.));
#8417=CARTESIAN_POINT('',(0.,0.,0.));
#8418=CARTESIAN_POINT('Origin',(-65.371725664246,-65.371725664246,20.));
#8419=CARTESIAN_POINT('',(-65.371725664246,-75.371725664246,20.));
#8420=CARTESIAN_POINT('Origin',(-65.371725664246,-65.371725664246,20.));
#8421=CARTESIAN_POINT('',(-65.371725664246,-75.371725664246,0.));
#8422=CARTESIAN_POINT('',(-65.371725664246,-75.371725664246,20.));
#8423=CARTESIAN_POINT('Origin',(-65.371725664246,-65.371725664246,0.));
#8424=CARTESIAN_POINT('Origin',(-83.0493951939097,-83.0493951939097,20.));
#8425=CARTESIAN_POINT('',(-83.0493951939097,-93.0493951939097,20.));
#8426=CARTESIAN_POINT('Origin',(-83.0493951939097,-83.0493951939097,20.));
#8427=CARTESIAN_POINT('',(-83.0493951939097,-93.0493951939097,0.));
#8428=CARTESIAN_POINT('',(-83.0493951939097,-93.0493951939097,20.));
#8429=CARTESIAN_POINT('Origin',(-83.0493951939097,-83.0493951939097,0.));
#8430=CARTESIAN_POINT('Origin',(-65.371725664246,65.371725664246,20.));
#8431=CARTESIAN_POINT('',(-75.371725664246,65.371725664246,20.));
#8432=CARTESIAN_POINT('Origin',(-65.371725664246,65.371725664246,20.));
#8433=CARTESIAN_POINT('',(-75.371725664246,65.371725664246,0.));
#8434=CARTESIAN_POINT('',(-75.371725664246,65.371725664246,20.));
#8435=CARTESIAN_POINT('Origin',(-65.371725664246,65.371725664246,0.));
#8436=CARTESIAN_POINT('Origin',(-83.0493951939097,83.0493951939097,20.));
#8437=CARTESIAN_POINT('',(-93.0493951939097,83.0493951939097,20.));
#8438=CARTESIAN_POINT('Origin',(-83.0493951939097,83.0493951939097,20.));
#8439=CARTESIAN_POINT('',(-93.0493951939097,83.0493951939097,0.));
#8440=CARTESIAN_POINT('',(-93.0493951939097,83.0493951939097,20.));
#8441=CARTESIAN_POINT('Origin',(-83.0493951939097,83.0493951939097,0.));
#8442=CARTESIAN_POINT('Origin',(65.371725664246,65.371725664246,20.));
#8443=CARTESIAN_POINT('',(65.371725664246,75.371725664246,20.));
#8444=CARTESIAN_POINT('Origin',(65.371725664246,65.371725664246,20.));
#8445=CARTESIAN_POINT('',(65.371725664246,75.371725664246,0.));
#8446=CARTESIAN_POINT('',(65.371725664246,75.371725664246,20.));
#8447=CARTESIAN_POINT('Origin',(65.371725664246,65.371725664246,0.));
#8448=CARTESIAN_POINT('Origin',(83.0493951939097,83.0493951939097,20.));
#8449=CARTESIAN_POINT('',(83.0493951939097,93.0493951939097,20.));
#8450=CARTESIAN_POINT('Origin',(83.0493951939097,83.0493951939097,20.));
#8451=CARTESIAN_POINT('',(83.0493951939097,93.0493951939097,0.));
#8452=CARTESIAN_POINT('',(83.0493951939097,93.0493951939097,20.));
#8453=CARTESIAN_POINT('Origin',(83.0493951939097,83.0493951939097,0.));
#8454=CARTESIAN_POINT('Origin',(83.0493951939097,-83.0493951939097,20.));
#8455=CARTESIAN_POINT('',(93.0493951939097,-83.0493951939097,20.));
#8456=CARTESIAN_POINT('Origin',(83.0493951939097,-83.0493951939097,20.));
#8457=CARTESIAN_POINT('',(93.0493951939097,-83.0493951939097,0.));
#8458=CARTESIAN_POINT('',(93.0493951939097,-83.0493951939097,20.));
#8459=CARTESIAN_POINT('Origin',(83.0493951939097,-83.0493951939097,0.));
#8460=CARTESIAN_POINT('Origin',(65.371725664246,-65.371725664246,20.));
#8461=CARTESIAN_POINT('',(75.371725664246,-65.371725664246,20.));
#8462=CARTESIAN_POINT('Origin',(65.371725664246,-65.371725664246,20.));
#8463=CARTESIAN_POINT('',(75.371725664246,-65.371725664246,0.));
#8464=CARTESIAN_POINT('',(75.371725664246,-65.371725664246,20.));
#8465=CARTESIAN_POINT('Origin',(65.371725664246,-65.371725664246,0.));
#8466=CARTESIAN_POINT('Origin',(-90.,90.,0.));
#8467=CARTESIAN_POINT('',(-100.,90.,20.));
#8468=CARTESIAN_POINT('',(-90.,100.,20.));
#8469=CARTESIAN_POINT('Origin',(-90.,90.,20.));
#8470=CARTESIAN_POINT('',(-90.,100.,0.));
#8471=CARTESIAN_POINT('',(-90.,100.,0.));
#8472=CARTESIAN_POINT('',(-100.,90.,0.));
#8473=CARTESIAN_POINT('Origin',(-90.,90.,0.));
#8474=CARTESIAN_POINT('',(-100.,90.,0.));
#8475=CARTESIAN_POINT('Origin',(-100.,100.,0.));
#8476=CARTESIAN_POINT('',(-100.,-90.,0.));
#8477=CARTESIAN_POINT('',(-100.,-100.,0.));
#8478=CARTESIAN_POINT('',(-100.,-90.,20.));
#8479=CARTESIAN_POINT('',(-100.,-90.,0.));
#8480=CARTESIAN_POINT('',(-100.,-100.,20.));
#8481=CARTESIAN_POINT('Origin',(0.,0.,0.));
#8482=CARTESIAN_POINT('',(90.,100.,0.));
#8483=CARTESIAN_POINT('',(-100.,100.,0.));
#8484=CARTESIAN_POINT('',(100.,90.,0.));
#8485=CARTESIAN_POINT('Origin',(90.,90.,0.));
#8486=CARTESIAN_POINT('',(100.,-90.,0.));
#8487=CARTESIAN_POINT('',(100.,100.,0.));
#8488=CARTESIAN_POINT('',(90.,-100.,0.));
#8489=CARTESIAN_POINT('Origin',(90.,-90.,0.));
#8490=CARTESIAN_POINT('',(-90.,-100.,0.));
#8491=CARTESIAN_POINT('',(100.,-100.,0.));
#8492=CARTESIAN_POINT('Origin',(-90.,-90.,0.));
#8493=CARTESIAN_POINT('Origin',(90.,90.,0.));
#8494=CARTESIAN_POINT('',(90.,100.,20.));
#8495=CARTESIAN_POINT('',(100.,90.,20.));
#8496=CARTESIAN_POINT('Origin',(90.,90.,20.));
#8497=CARTESIAN_POINT('',(100.,90.,0.));
#8498=CARTESIAN_POINT('',(90.,100.,0.));
#8499=CARTESIAN_POINT('Origin',(100.,-100.,0.));
#8500=CARTESIAN_POINT('',(100.,-90.,20.));
#8501=CARTESIAN_POINT('',(100.,100.,20.));
#8502=CARTESIAN_POINT('',(100.,-90.,0.));
#8503=CARTESIAN_POINT('Origin',(90.,-90.,0.));
#8504=CARTESIAN_POINT('',(90.,-100.,20.));
#8505=CARTESIAN_POINT('Origin',(90.,-90.,20.));
#8506=CARTESIAN_POINT('',(90.,-100.,0.));
#8507=CARTESIAN_POINT('Origin',(-90.,-90.,0.));
#8508=CARTESIAN_POINT('',(-90.,-100.,20.));
#8509=CARTESIAN_POINT('Origin',(-90.,-90.,20.));
#8510=CARTESIAN_POINT('',(-90.,-100.,0.));
#8511=CARTESIAN_POINT('Origin',(-100.,-100.,0.));
#8512=CARTESIAN_POINT('',(100.,-100.,20.));
#8513=CARTESIAN_POINT('Origin',(100.,100.,0.));
#8514=CARTESIAN_POINT('',(-100.,100.,20.));
#8515=CARTESIAN_POINT('Origin',(0.,0.,20.));
#10109=UNCERTAINTY_MEASURE_WITH_UNIT(LENGTH_MEASURE(0.01),#10132,
'DISTANCE_ACCURACY_VALUE',
'Maximum model space distance between geometric entities at asserted c
onnectivities');
#10119=UNCERTAINTY_MEASURE_WITH_UNIT(LENGTH_MEASURE(0.01),#10132,
'DISTANCE_ACCURACY_VALUE',
'Maximum model space distance between geometric entities at asserted c
onnectivities');
#10121=(
GEOMETRIC_REPRESENTATION_CONTEXT(3)
GLOBAL_UNCERTAINTY_ASSIGNED_CONTEXT((#10109))
GLOBAL_UNIT_ASSIGNED_CONTEXT((#10132,#10134,#10135))
REPRESENTATION_CONTEXT('','3D')
);
#10131=(
GEOMETRIC_REPRESENTATION_CONTEXT(3)
GLOBAL_UNCERTAINTY_ASSIGNED_CONTEXT((#10119))
GLOBAL_UNIT_ASSIGNED_CONTEXT((#10132,#10134,#10135))
REPRESENTATION_CONTEXT('','3D')
);
#10132=(
LENGTH_UNIT()
NAMED_UNIT(*)
SI_UNIT(.MILLI.,.METRE.)
);
#10134=(
NAMED_UNIT(*)
PLANE_ANGLE_UNIT()
SI_UNIT($,.RADIAN.)
);
#10135=(
NAMED_UNIT(*)
SI_UNIT($,.STERADIAN.)
SOLID_ANGLE_UNIT()
);
#10137=SHAPE_DEFINITION_REPRESENTATION(#10148,#10169);
#10148=PRODUCT_DEFINITION_SHAPE('',$,#10181);
#10169=SHAPE_REPRESENTATION('',(#6001),#10121);
#10179=PRODUCT_DEFINITION_CONTEXT('part definition',#10214,'design');
#10181=PRODUCT_DEFINITION('Base','Base',#10192,#10179);
#10192=PRODUCT_DEFINITION_FORMATION('',$,#10217);
#10214=APPLICATION_CONTEXT(
'Core Data for Automotive Mechanical Design Process');
#10215=PRODUCT_CONTEXT('part definition',#10214,'mechanical');
#10217=PRODUCT('Base','Base',$,(#10215));
#10241=COLOUR_RGB('Dark Blue',0.08,0.2,0.34);
#10242=FILL_AREA_STYLE_COLOUR('',#10241);
#10243=FILL_AREA_STYLE('',(#10242));
#10244=SURFACE_STYLE_FILL_AREA(#10243);
#10245=SURFACE_SIDE_STYLE('',(#10244));
#10246=SURFACE_STYLE_USAGE(.BOTH.,#10245);
#10247=PRESENTATION_STYLE_ASSIGNMENT((#10246));
ENDSEC;
END-ISO-10303-21;
